ISO-10303-21;
HEADER;
FILE_DESCRIPTION (('STEP AP203'),
    '1' );
FILE_NAME ('bench vise6_2-.step',
    '2026-10-07T23:37:23',
    ( '' ),
    ( '' ),
    'SwSTEP 2.0',
    'SolidWorks 2024',
    '' );
FILE_SCHEMA (( 'AUTOMOTIVE_DESIGN' ));
ENDSEC;

DATA;
#302=VECTOR ( 'NONE', #7166, 39.37007874015748143 ) ;
#303=PRODUCT_DEFINITION_FORMATION_WITH_SPECIFIED_SOURCE ( 'ANY', '', #4564, .NOT_KNOWN. ) ;
#339=ORIENTED_EDGE ( 'NONE', *, *, #1049, .T. ) ;
#552=CARTESIAN_POINT ( 'NONE',  ( 2.537499998660271761, 3.737500000000002043, 2.790532913385826763 ) ) ;
#576=AXIS2_PLACEMENT_3D ( 'NONE', #6538, #4671, #3408 ) ;
#588=( GEOMETRIC_REPRESENTATION_CONTEXT ( 3 ) GLOBAL_UNCERTAINTY_ASSIGNED_CONTEXT ( ( #4715 ) ) GLOBAL_UNIT_ASSIGNED_CONTEXT ( ( #6311, #3231, #3119 ) ) REPRESENTATION_CONTEXT ( 'NONE', 'WORKASPACE' ) );
#836=ADVANCED_FACE ( 'NONE', ( #1661 ), #6633, .T. ) ;
#896=DIRECTION ( 'NONE',  ( -0.000000000000000000, -0.000000000000000000, 1.000000000000000000 ) ) ;
#905=APPLICATION_CONTEXT ( 'configuration controlled 3d designs of mechanical parts and assemblies' ) ;
#985=CARTESIAN_POINT ( 'NONE',  ( 2.537499998660271761, 3.550000000000001155, 2.790532913385826763 ) ) ;
#1037=PLANE ( 'NONE',  #576 ) ;
#1049=EDGE_CURVE ( 'NONE', #1962, #3600, #3677, .T. ) ;
#1241=ADVANCED_BREP_SHAPE_REPRESENTATION ( '', ( #7800, #7272 ), #588 ) ;
#1470=EDGE_CURVE ( 'NONE', #3236, #1962, #5866, .T. ) ;
#1545=AXIS2_PLACEMENT_3D ( 'NONE', #5081, #3845, #3805 ) ;
#1661=FACE_OUTER_BOUND ( 'NONE', #3678, .T. ) ;
#1675=ORIENTED_EDGE ( 'NONE', *, *, #5023, .F. ) ;
#1897=CLOSED_SHELL ( 'NONE', ( #3279, #836, #5843, #5088 ) ) ;
#1962=VERTEX_POINT ( 'NONE', #6389 ) ;
#1994=CARTESIAN_POINT ( 'NONE',  ( 2.724999998660272205, 3.550000000000001155, 0.3883559095726499266 ) ) ;
#1997=CARTESIAN_POINT ( 'NONE',  ( 2.537499998660271761, 3.550000000000001155, 0.3883559095726499266 ) ) ;
#2025=ORIENTED_EDGE ( 'NONE', *, *, #5083, .F. ) ;
#2150=CARTESIAN_POINT ( 'NONE',  ( 2.349999998660270872, 3.550000000000001155, 2.790532913385826763 ) ) ;
#2201=SHAPE_DEFINITION_REPRESENTATION ( #5489, #6040 ) ;
#2330=DIRECTION ( 'NONE',  ( 0.000000000000000000, -0.000000000000000000, 1.000000000000000000 ) ) ;
#2605=CARTESIAN_POINT ( 'NONE',  ( 2.349999998660270872, 3.550000000000001155, 0.3883559095726499266 ) ) ;
#2765=EDGE_LOOP ( 'NONE', ( #2025, #5933 ) ) ;
#2794=AXIS2_PLACEMENT_3D ( 'NONE', #7179, #5821, #5317 ) ;
#2810=AXIS2_PLACEMENT_3D ( 'NONE', #552, #2330, #3052 ) ;
#2936=CARTESIAN_POINT ( 'NONE',  ( 2.537499998660271761, 3.550000000000001155, 0.3883559095726499266 ) ) ;
#3020=EDGE_CURVE ( 'NONE', #3236, #3210, #7811, .T. ) ;
#3052=DIRECTION ( 'NONE',  ( 1.000000000000000000, 0.000000000000000000, -0.000000000000000000 ) ) ;
#3119=( NAMED_UNIT ( * ) SI_UNIT ( $, .STERADIAN. ) SOLID_ANGLE_UNIT ( ) );
#3134=ORIENTED_EDGE ( 'NONE', *, *, #3020, .T. ) ;
#3138=ORIENTED_EDGE ( 'NONE', *, *, #5023, .T. ) ;
#3200=CIRCLE ( 'NONE', #4104, 0.1875000000000006661 ) ;
#3210=VERTEX_POINT ( 'NONE', #2605 ) ;
#3231=( NAMED_UNIT ( * ) PLANE_ANGLE_UNIT ( ) SI_UNIT ( $, .RADIAN. ) );
#3236=VERTEX_POINT ( 'NONE', #2150 ) ;
#3279=ADVANCED_FACE ( 'NONE', ( #6577 ), #3316, .T. ) ;
#3316=CYLINDRICAL_SURFACE ( 'NONE', #2794, 0.1875000000000006661 ) ;
#3408=DIRECTION ( 'NONE',  ( -1.000000000000000000, 0.000000000000000000, -0.000000000000000000 ) ) ;
#3447=ORIENTED_EDGE ( 'NONE', *, *, #5083, .T. ) ;
#3462=DIRECTION ( 'NONE',  ( -1.000000000000000000, 0.000000000000000000, 0.000000000000000000 ) ) ;
#3480=DIRECTION ( 'NONE',  ( 0.000000000000000000, 0.000000000000000000, -1.000000000000000000 ) ) ;
#3598=DIRECTION ( 'NONE',  ( -0.000000000000000000, -0.000000000000000000, 1.000000000000000000 ) ) ;
#3600=VERTEX_POINT ( 'NONE', #1994 ) ;
#3677=LINE ( 'NONE', #5632, #4137 ) ;
#3678=EDGE_LOOP ( 'NONE', ( #5613, #3138, #3134, #3447 ) ) ;
#3736=CARTESIAN_POINT ( 'NONE',  ( 0.000000000000000000, 0.000000000000000000, 0.000000000000000000 ) ) ;
#3805=DIRECTION ( 'NONE',  ( -1.000000000000000000, 0.000000000000000000, 0.000000000000000000 ) ) ;
#3845=DIRECTION ( 'NONE',  ( 0.000000000000000000, 0.000000000000000000, -1.000000000000000000 ) ) ;
#4104=AXIS2_PLACEMENT_3D ( 'NONE', #2936, #3598, #6172 ) ;
#4137=VECTOR ( 'NONE', #6297, 39.37007874015748143 ) ;
#4222=CIRCLE ( 'NONE', #6464, 0.1875000000000006661 ) ;
#4436=DIMENSIONAL_EXPONENTS ( 1.000000000000000000, 0.000000000000000000, 0.000000000000000000, 0.000000000000000000, 0.000000000000000000, 0.000000000000000000, 0.000000000000000000 ) ;
#4564=PRODUCT ( 'bench vise6_2-', 'bench vise6_2-', '', ( #6558 ) ) ;
#4671=DIRECTION ( 'NONE',  ( 0.000000000000000000, 0.000000000000000000, -1.000000000000000000 ) ) ;
#4715=UNCERTAINTY_MEASURE_WITH_UNIT (LENGTH_MEASURE( 1.000000000000000082E-05 ), #6311, 'distance_accuracy_value', 'NONE');
#4796=ORIENTED_EDGE ( 'NONE', *, *, #3020, .F. ) ;
#5023=EDGE_CURVE ( 'NONE', #1962, #3236, #6865, .T. ) ;
#5033=( LENGTH_UNIT ( ) NAMED_UNIT ( * ) SI_UNIT ( $, .METRE. ) );
#5075=SHAPE_REPRESENTATION_RELATIONSHIP ( 'NONE' , 'NONE' ,  #6040, #1241 ) ;
#5081=CARTESIAN_POINT ( 'NONE',  ( 2.537499998660271761, 3.550000000000001155, 2.790532913385826763 ) ) ;
#5083=EDGE_CURVE ( 'NONE', #3210, #3600, #3200, .T. ) ;
#5088=ADVANCED_FACE ( 'N', ( #5509 ), #5553, .T. ) ;
#5114=ORIENTED_EDGE ( 'NONE', *, *, #7643, .T. ) ;
#5294=DIRECTION ( 'NONE',  ( 0.000000000000000000, 0.000000000000000000, -1.000000000000000000 ) ) ;
#5317=DIRECTION ( 'NONE',  ( -1.000000000000000000, 0.000000000000000000, 0.000000000000000000 ) ) ;
#5370=ORIENTED_EDGE ( 'NONE', *, *, #1470, .T. ) ;
#5489=PRODUCT_DEFINITION_SHAPE ( 'NONE', 'NONE',  #7978 ) ;
#5509=FACE_OUTER_BOUND ( 'NONE', #7274, .T. ) ;
#5553=PLANE ( 'NONE',  #2810 ) ;
#5613=ORIENTED_EDGE ( 'NONE', *, *, #1049, .F. ) ;
#5618=DIRECTION ( 'NONE',  ( 1.000000000000000000, 0.000000000000000000, 0.000000000000000000 ) ) ;
#5632=CARTESIAN_POINT ( 'NONE',  ( 2.724999998660272205, 3.550000000000001155, 2.790532913385826763 ) ) ;
#5732=DIRECTION ( 'NONE',  ( -1.000000000000000000, 0.000000000000000000, 0.000000000000000000 ) ) ;
#5821=DIRECTION ( 'NONE',  ( 0.000000000000000000, 0.000000000000000000, -1.000000000000000000 ) ) ;
#5843=ADVANCED_FACE ( 'NONE', ( #5946 ), #1037, .T. ) ;
#5866=CIRCLE ( 'NONE', #1545, 0.1875000000000006661 ) ;
#5933=ORIENTED_EDGE ( 'NONE', *, *, #7643, .F. ) ;
#5946=FACE_OUTER_BOUND ( 'NONE', #2765, .T. ) ;
#5977=AXIS2_PLACEMENT_3D ( 'NONE', #7851, #5294, #3462 ) ;
#6040=SHAPE_REPRESENTATION ( 'bench vise6_2-', ( #7272 ), #588 ) ;
#6172=DIRECTION ( 'NONE',  ( -1.000000000000000000, 0.000000000000000000, 0.000000000000000000 ) ) ;
#6237=DIRECTION ( 'NONE',  ( 0.000000000000000000, 0.000000000000000000, 1.000000000000000000 ) ) ;
#6297=DIRECTION ( 'NONE',  ( 0.000000000000000000, 0.000000000000000000, -1.000000000000000000 ) ) ;
#6311=( CONVERSION_BASED_UNIT ( 'INCH', #7574 ) LENGTH_UNIT ( ) NAMED_UNIT ( #4436 ) );
#6389=CARTESIAN_POINT ( 'NONE',  ( 2.724999998660272205, 3.550000000000001155, 2.790532913385826763 ) ) ;
#6464=AXIS2_PLACEMENT_3D ( 'NONE', #1997, #896, #5732 ) ;
#6538=CARTESIAN_POINT ( 'NONE',  ( 2.537499998660271761, 3.550000000000001155, 0.3883559095726498156 ) ) ;
#6558=MECHANICAL_CONTEXT ( 'NONE', #905, 'mechanical' ) ;
#6577=FACE_OUTER_BOUND ( 'NONE', #6793, .T. ) ;
#6633=CYLINDRICAL_SURFACE ( 'NONE', #5977, 0.1875000000000006661 ) ;
#6739=AXIS2_PLACEMENT_3D ( 'NONE', #985, #3480, #7772 ) ;
#6793=EDGE_LOOP ( 'NONE', ( #5370, #339, #5114, #4796 ) ) ;
#6865=CIRCLE ( 'NONE', #6739, 0.1875000000000006661 ) ;
#7106=DESIGN_CONTEXT ( 'detailed design', #7415, 'design' ) ;
#7166=DIRECTION ( 'NONE',  ( 0.000000000000000000, 0.000000000000000000, -1.000000000000000000 ) ) ;
#7179=CARTESIAN_POINT ( 'NONE',  ( 2.537499998660271761, 3.550000000000001155, 2.790532913385826763 ) ) ;
#7272=AXIS2_PLACEMENT_3D ( 'NONE', #3736, #6237, #5618 ) ;
#7274=EDGE_LOOP ( 'NONE', ( #8136, #1675 ) ) ;
#7415=APPLICATION_CONTEXT ( 'configuration controlled 3d designs of mechanical parts and assemblies' ) ;
#7574=LENGTH_MEASURE_WITH_UNIT ( LENGTH_MEASURE( 0.02539999999999999897 ), #5033 );
#7643=EDGE_CURVE ( 'NONE', #3600, #3210, #4222, .T. ) ;
#7728=CARTESIAN_POINT ( 'NONE',  ( 2.349999998660270872, 3.550000000000001155, 2.790532913385826763 ) ) ;
#7772=DIRECTION ( 'NONE',  ( -1.000000000000000000, 0.000000000000000000, 0.000000000000000000 ) ) ;
#7800=MANIFOLD_SOLID_BREP ( 'Imported1', #1897 ) ;
#7811=LINE ( 'NONE', #7728, #302 ) ;
#7851=CARTESIAN_POINT ( 'NONE',  ( 2.537499998660271761, 3.550000000000001155, 2.790532913385826763 ) ) ;
#7978=PRODUCT_DEFINITION ( 'UNKNOWN', '', #303, #7106 ) ;
#8136=ORIENTED_EDGE ( 'NONE', *, *, #1470, .F. ) ;
#8220=COLOUR_RGB('Slate Gray', 0.72549020, 0.75294118, 0.79215686);
#8221=FILL_AREA_STYLE_COLOUR('',#8220);
#8222=FILL_AREA_STYLE('',(#8221));
#8223=SURFACE_STYLE_FILL_AREA(#8222);
#8224=SURFACE_SIDE_STYLE('',(#8223));
#8225=SURFACE_STYLE_USAGE(.BOTH.,#8224);
#8226=PRESENTATION_STYLE_ASSIGNMENT((#8225));
#8245=STYLED_ITEM('',(#8226),#7800);
#8246=MECHANICAL_DESIGN_GEOMETRIC_PRESENTATION_REPRESENTATION('',(#8245),#588);
ENDSEC;
END-ISO-10303-21;
